ISO-10303-21;
HEADER;
FILE_DESCRIPTION (('STEP AP214'),
    '1' );
FILE_NAME ('output shaft.step',
    '2026-09-30T12:41:04',
    ( '' ),
    ( '' ),
    'SwSTEP 2.0',
    'SolidWorks 2026',
    '' );
FILE_SCHEMA (( 'AUTOMOTIVE_DESIGN' ));
ENDSEC;

DATA;
#64=AXIS2_PLACEMENT_3D ( 'NONE', #6293, #21927, #48124 ) ;
#74=CARTESIAN_POINT ( 'NONE',  ( 0.000000000000000000, -132.5000000000000000, -40.00000000000000711 ) ) ;
#250=EDGE_LOOP ( 'NONE', ( #16090, #5934 ) ) ;
#290=DIRECTION ( 'NONE',  ( -0.000000000000000000, -0.000000000000000000, -1.000000000000000000 ) ) ;
#311=CARTESIAN_POINT ( 'NONE',  ( -12.49999999999999822, -120.0000000000000000, 125.0000000000000000 ) ) ;
#493=VECTOR ( 'NONE', #19133, 1000.000000000000000 ) ;
#498=EDGE_LOOP ( 'NONE', ( #18860, #40919, #13713 ) ) ;
#644=ORIENTED_EDGE ( 'NONE', *, *, #19554, .F. ) ;
#718=UNCERTAINTY_MEASURE_WITH_UNIT (LENGTH_MEASURE( 1.000000000000000082E-05 ), #46005, 'distance_accuracy_value', 'NONE');
#832=ORIENTED_EDGE ( 'NONE', *, *, #10836, .F. ) ;
#996=CARTESIAN_POINT ( 'NONE',  ( -12.50000000000000000, -132.5000000000000000, -40.00000000000000000 ) ) ;
#1208=( NAMED_UNIT ( * ) PLANE_ANGLE_UNIT ( ) SI_UNIT ( $, .RADIAN. ) );
#1226=SHAPE_REPRESENTATION ( 'output shaft', ( #11636 ), #38234 ) ;
#1299=LINE ( 'NONE', #311, #9038 ) ;
#1376=DIRECTION ( 'NONE',  ( 1.000000000000000000, 0.000000000000000000, 0.000000000000000000 ) ) ;
#1427=AXIS2_PLACEMENT_3D ( 'NONE', #7158, #290, #22077 ) ;
#1848=EDGE_LOOP ( 'NONE', ( #21536, #11227, #33537, #5622, #47988 ) ) ;
#1943=ORIENTED_EDGE ( 'NONE', *, *, #20789, .F. ) ;
#2471=SURFACE_SIDE_STYLE ('',( #25214 ) ) ;
#2608=LINE ( 'NONE', #27884, #25894 ) ;
#2651=ORIENTED_EDGE ( 'NONE', *, *, #6841, .F. ) ;
#2727=CARTESIAN_POINT ( 'NONE',  ( -12.49999999999999822, -120.0000000000000000, 125.0000000000000000 ) ) ;
#2796=ORIENTED_EDGE ( 'NONE', *, *, #25243, .T. ) ;
#3024=EDGE_LOOP ( 'NONE', ( #8311, #644, #44359, #28204, #41349, #33885 ) ) ;
#3194=DIRECTION ( 'NONE',  ( 0.000000000000000000, 0.000000000000000000, 1.000000000000000000 ) ) ;
#3251=VECTOR ( 'NONE', #29052, 1000.000000000000000 ) ;
#3659=DIRECTION ( 'NONE',  ( -1.000000000000000000, 0.000000000000000000, -0.000000000000000000 ) ) ;
#3667=DIRECTION ( 'NONE',  ( 1.000000000000000000, 0.000000000000000000, 0.000000000000000000 ) ) ;
#3763=ORIENTED_EDGE ( 'NONE', *, *, #35214, .T. ) ;
#3802=ORIENTED_EDGE ( 'NONE', *, *, #27807, .T. ) ;
#3816=ADVANCED_FACE ( 'NONE', ( #32674 ), #13854, .F. ) ;
#3839=CARTESIAN_POINT ( 'NONE',  ( -12.50000000000000000, -107.5000000000000000, 40.00000000000000000 ) ) ;
#3899=PLANE ( 'NONE',  #9617 ) ;
#3929=ORIENTED_EDGE ( 'NONE', *, *, #38470, .F. ) ;
#3977=FACE_OUTER_BOUND ( 'NONE', #41368, .T. ) ;
#4121=DIRECTION ( 'NONE',  ( -1.000000000000000000, 0.000000000000000000, 0.000000000000000000 ) ) ;
#4123=VERTEX_POINT ( 'NONE', #6657 ) ;
#4270=CARTESIAN_POINT ( 'NONE',  ( 0.000000000000000000, 0.000000000000000000, -40.00000000000000000 ) ) ;
#4401=CARTESIAN_POINT ( 'NONE',  ( 0.000000000000000000, -120.0000000000000000, 40.00000000000000711 ) ) ;
#4409=AXIS2_PLACEMENT_3D ( 'NONE', #25251, #43160, #25021 ) ;
#4637=UNCERTAINTY_MEASURE_WITH_UNIT (LENGTH_MEASURE( 1.000000000000000082E-05 ), #47711, 'distance_accuracy_value', 'NONE');
#4760=ORIENTED_EDGE ( 'NONE', *, *, #27976, .T. ) ;
#4834=ORIENTED_EDGE ( 'NONE', *, *, #19727, .F. ) ;
#5114=ADVANCED_FACE ( 'NONE', ( #48077 ), #7197, .T. ) ;
#5186=AXIS2_PLACEMENT_3D ( 'NONE', #45317, #45552, #11796 ) ;
#5318=VERTEX_POINT ( 'NONE', #24301 ) ;
#5406=LINE ( 'NONE', #20563, #15714 ) ;
#5581=CARTESIAN_POINT ( 'NONE',  ( 12.50000000000000000, -132.5000000000000000, -40.00000000000000000 ) ) ;
#5613=VECTOR ( 'NONE', #43614, 1000.000000000000000 ) ;
#5622=ORIENTED_EDGE ( 'NONE', *, *, #11274, .F. ) ;
#5652=EDGE_CURVE ( 'NONE', #25578, #23496, #11318, .T. ) ;
#5679=DIRECTION ( 'NONE',  ( 0.000000000000000000, 0.000000000000000000, -1.000000000000000000 ) ) ;
#5695=ORIENTED_EDGE ( 'NONE', *, *, #41246, .T. ) ;
#5934=ORIENTED_EDGE ( 'NONE', *, *, #17328, .F. ) ;
#5935=DIRECTION ( 'NONE',  ( -1.000000000000000000, 0.000000000000000000, 0.000000000000000000 ) ) ;
#6093=DIRECTION ( 'NONE',  ( -0.000000000000000000, -1.000000000000000000, -0.000000000000000000 ) ) ;
#6165=FILL_AREA_STYLE ('',( #44326 ) ) ;
#6293=CARTESIAN_POINT ( 'NONE',  ( -12.50000000000000000, -132.5000000000000000, 40.00000000000000000 ) ) ;
#6382=AXIS2_PLACEMENT_3D ( 'NONE', #41814, #46199, #38627 ) ;
#6508=ORIENTED_EDGE ( 'NONE', *, *, #27807, .F. ) ;
#6556=AXIS2_PLACEMENT_3D ( 'NONE', #24763, #39934, #35283 ) ;
#6608=LINE ( 'NONE', #47701, #17267 ) ;
#6619=DIRECTION ( 'NONE',  ( 0.000000000000000000, 0.000000000000000000, 1.000000000000000000 ) ) ;
#6657=CARTESIAN_POINT ( 'NONE',  ( -12.50000000000000000, -107.5000000000000000, -40.00000000000000000 ) ) ;
#6688=DIRECTION ( 'NONE',  ( -1.000000000000000000, -0.000000000000000000, -0.000000000000000000 ) ) ;
#6694=VERTEX_POINT ( 'NONE', #39981 ) ;
#6697=EDGE_CURVE ( 'NONE', #34109, #35947, #25027, .T. ) ;
#6714=VERTEX_POINT ( 'NONE', #47543 ) ;
#6782=CARTESIAN_POINT ( 'NONE',  ( 0.000000000000000000, 0.000000000000000000, -40.00000000000000000 ) ) ;
#6841=EDGE_CURVE ( 'NONE', #24524, #25578, #48272, .T. ) ;
#6907=ADVANCED_FACE ( 'NONE', ( #37258 ), #41190, .F. ) ;
#6910=CARTESIAN_POINT ( 'NONE',  ( 0.000000000000000000, -120.0000000000000000, -125.0000000000000000 ) ) ;
#6942=ORIENTED_EDGE ( 'NONE', *, *, #42710, .T. ) ;
#7090=SURFACE_STYLE_FILL_AREA ( #40626 ) ;
#7158=CARTESIAN_POINT ( 'NONE',  ( 0.000000000000000000, -120.0000000000000000, 125.0000000000000000 ) ) ;
#7197=CYLINDRICAL_SURFACE ( 'NONE', #36762, 12.49999999999999822 ) ;
#7368=CARTESIAN_POINT ( 'NONE',  ( 0.000000000000000000, -120.0000000000000000, -125.0000000000000000 ) ) ;
#7493=ORIENTED_EDGE ( 'NONE', *, *, #38470, .T. ) ;
#7546=ORIENTED_EDGE ( 'NONE', *, *, #10924, .T. ) ;
#7632=CARTESIAN_POINT ( 'NONE',  ( -12.50000000000000000, -132.5000000000000000, 40.00000000000000000 ) ) ;
#7865=DIRECTION ( 'NONE',  ( 0.000000000000000000, 0.000000000000000000, 1.000000000000000000 ) ) ;
#7879=STYLED_ITEM ( 'NONE', ( #13752 ), #19912 ) ;
#7974=VERTEX_POINT ( 'NONE', #74 ) ;
#7996=CYLINDRICAL_SURFACE ( 'NONE', #22060, 12.49999999999999822 ) ;
#8056=( NAMED_UNIT ( * ) SI_UNIT ( $, .STERADIAN. ) SOLID_ANGLE_UNIT ( ) );
#8114=CARTESIAN_POINT ( 'NONE',  ( -12.50000000000000000, -132.5000000000000000, 40.00000000000000000 ) ) ;
#8311=ORIENTED_EDGE ( 'NONE', *, *, #42710, .F. ) ;
#8579=DIRECTION ( 'NONE',  ( 1.000000000000000000, 0.000000000000000000, 0.000000000000000000 ) ) ;
#8624=DIRECTION ( 'NONE',  ( 0.000000000000000000, 0.000000000000000000, -1.000000000000000000 ) ) ;
#8675=DIRECTION ( 'NONE',  ( 0.000000000000000000, 0.000000000000000000, -1.000000000000000000 ) ) ;
#8848=SHAPE_DEFINITION_REPRESENTATION ( #32384, #1226 ) ;
#9038=VECTOR ( 'NONE', #19158, 1000.000000000000000 ) ;
#9093=ORIENTED_EDGE ( 'NONE', *, *, #5652, .F. ) ;
#9443=CIRCLE ( 'NONE', #36032, 12.49999999999999822 ) ;
#9447=VECTOR ( 'NONE', #39709, 1000.000000000000000 ) ;
#9617=AXIS2_PLACEMENT_3D ( 'NONE', #22265, #37190, #3659 ) ;
#9949=ADVANCED_FACE ( 'NONE', ( #35622 ), #42971, .F. ) ;
#9989=VERTEX_POINT ( 'NONE', #24351 ) ;
#10152=VECTOR ( 'NONE', #1376, 1000.000000000000000 ) ;
#10173=CIRCLE ( 'NONE', #26608, 12.49999999999999822 ) ;
#10432=ORIENTED_EDGE ( 'NONE', *, *, #31700, .F. ) ;
#10580=DIRECTION ( 'NONE',  ( -1.000000000000000000, 0.000000000000000000, -0.000000000000000000 ) ) ;
#10628=ORIENTED_EDGE ( 'NONE', *, *, #34174, .F. ) ;
#10694=FACE_OUTER_BOUND ( 'NONE', #3024, .T. ) ;
#10697=AXIS2_PLACEMENT_3D ( 'NONE', #4401, #34228, #42075 ) ;
#10706=CARTESIAN_POINT ( 'NONE',  ( -12.50000000000000000, -132.5000000000000000, 40.00000000000000000 ) ) ;
#10777=FILL_AREA_STYLE_COLOUR ( '', #14784 ) ;
#10836=EDGE_CURVE ( 'NONE', #9989, #6694, #5406, .T. ) ;
#10924=EDGE_CURVE ( 'NONE', #4123, #37702, #6608, .T. ) ;
#11112=CARTESIAN_POINT ( 'NONE',  ( 12.49999999999999822, -120.0000000000000000, 125.0000000000000000 ) ) ;
#11123=DIRECTION ( 'NONE',  ( 0.000000000000000000, -1.000000000000000000, 0.000000000000000000 ) ) ;
#11227=ORIENTED_EDGE ( 'NONE', *, *, #6697, .T. ) ;
#11274=EDGE_CURVE ( 'NONE', #24524, #13681, #42746, .T. ) ;
#11293=FACE_OUTER_BOUND ( 'NONE', #250, .T. ) ;
#11318=LINE ( 'NONE', #7632, #31564 ) ;
#11349=CARTESIAN_POINT ( 'NONE',  ( 0.000000000000000000, 0.000000000000000000, -40.00000000000000000 ) ) ;
#11557=CARTESIAN_POINT ( 'NONE',  ( 0.000000000000000000, -120.0000000000000000, 40.00000000000000711 ) ) ;
#11636=AXIS2_PLACEMENT_3D ( 'NONE', #13959, #6619, #3667 ) ;
#11667=LINE ( 'NONE', #29540, #44129 ) ;
#11796=DIRECTION ( 'NONE',  ( 0.000000000000000000, 0.000000000000000000, 1.000000000000000000 ) ) ;
#11820=DIRECTION ( 'NONE',  ( 0.000000000000000000, 1.000000000000000000, 0.000000000000000000 ) ) ;
#12145=CARTESIAN_POINT ( 'NONE',  ( 0.000000000000000000, -120.0000000000000000, -40.00000000000000711 ) ) ;
#12248=ORIENTED_EDGE ( 'NONE', *, *, #28466, .T. ) ;
#12250=VECTOR ( 'NONE', #6093, 1000.000000000000000 ) ;
#12326=CARTESIAN_POINT ( 'NONE',  ( 0.000000000000000000, -120.0000000000000000, -40.00000000000000711 ) ) ;
#12399=ORIENTED_EDGE ( 'NONE', *, *, #38888, .T. ) ;
#12473=ORIENTED_EDGE ( 'NONE', *, *, #17328, .T. ) ;
#12650=CIRCLE ( 'NONE', #14212, 12.49999999999999822 ) ;
#13259=CIRCLE ( 'NONE', #19487, 12.49999999999999822 ) ;
#13437=DIRECTION ( 'NONE',  ( -1.000000000000000000, -0.000000000000000000, -0.000000000000000000 ) ) ;
#13492=ADVANCED_FACE ( 'NONE', ( #23181 ), #7996, .T. ) ;
#13506=AXIS2_PLACEMENT_3D ( 'NONE', #36813, #11123, #22386 ) ;
#13622=EDGE_LOOP ( 'NONE', ( #26938, #27019, #35181, #26155, #22976, #1943 ) ) ;
#13681=VERTEX_POINT ( 'NONE', #43944 ) ;
#13713=ORIENTED_EDGE ( 'NONE', *, *, #14915, .F. ) ;
#13752=PRESENTATION_STYLE_ASSIGNMENT (( #40644 ) ) ;
#13854=PLANE ( 'NONE',  #16883 ) ;
#13887=FACE_OUTER_BOUND ( 'NONE', #48109, .T. ) ;
#13959=CARTESIAN_POINT ( 'NONE',  ( 0.000000000000000000, 0.000000000000000000, 0.000000000000000000 ) ) ;
#13975=( NAMED_UNIT ( * ) PLANE_ANGLE_UNIT ( ) SI_UNIT ( $, .RADIAN. ) );
#14129=AXIS2_PLACEMENT_3D ( 'NONE', #46864, #20187, #35108 ) ;
#14212=AXIS2_PLACEMENT_3D ( 'NONE', #7368, #3194, #32814 ) ;
#14329=ORIENTED_EDGE ( 'NONE', *, *, #18240, .T. ) ;
#14639=CARTESIAN_POINT ( 'NONE',  ( -12.50000000000000000, -132.5000000000000000, 40.00000000000000000 ) ) ;
#14659=AXIS2_PLACEMENT_3D ( 'NONE', #40918, #21816, #10580 ) ;
#14684=DIRECTION ( 'NONE',  ( -1.000000000000000000, -0.000000000000000000, -0.000000000000000000 ) ) ;
#14784=COLOUR_RGB ( '', 0.31764706, 0.68627451, 0.89019608) ;
#14915=EDGE_CURVE ( 'NONE', #17845, #4123, #20287, .T. ) ;
#14964=AXIS2_PLACEMENT_3D ( 'NONE', #22566, #29173, #38718 ) ;
#15263=AXIS2_PLACEMENT_3D ( 'NONE', #17943, #47802, #44150 ) ;
#15269=EDGE_LOOP ( 'NONE', ( #3763, #22990, #7493 ) ) ;
#15386=ADVANCED_FACE ( 'NONE', ( #37029 ), #40702, .T. ) ;
#15704=ADVANCED_FACE ( 'NONE', ( #43124 ), #20851, .F. ) ;
#15714=VECTOR ( 'NONE', #42621, 1000.000000000000000 ) ;
#15727=CIRCLE ( 'NONE', #14964, 12.49999999999999822 ) ;
#15835=ORIENTED_EDGE ( 'NONE', *, *, #10836, .T. ) ;
#15859=ORIENTED_EDGE ( 'NONE', *, *, #6841, .T. ) ;
#15894=SHAPE_REPRESENTATION_RELATIONSHIP ( 'NONE' , 'NONE' ,  #1226, #38066 ) ;
#16090=ORIENTED_EDGE ( 'NONE', *, *, #28466, .F. ) ;
#16241=CARTESIAN_POINT ( 'NONE',  ( 12.50000000000000000, -132.5000000000000000, 40.00000000000000000 ) ) ;
#16544=VERTEX_POINT ( 'NONE', #38554 ) ;
#16883=AXIS2_PLACEMENT_3D ( 'NONE', #40745, #21416, #47600 ) ;
#16900=ORIENTED_EDGE ( 'NONE', *, *, #44715, .F. ) ;
#16975=ADVANCED_FACE ( 'NONE', ( #40252 ), #21636, .T. ) ;
#17062=CARTESIAN_POINT ( 'NONE',  ( 12.50000000000000000, -120.0000000000000000, 40.00000000000000711 ) ) ;
#17092=EDGE_CURVE ( 'NONE', #39765, #24524, #1299, .T. ) ;
#17207=ORIENTED_EDGE ( 'NONE', *, *, #41842, .F. ) ;
#17267=VECTOR ( 'NONE', #28870, 1000.000000000000000 ) ;
#17328=EDGE_CURVE ( 'NONE', #28782, #37765, #12650, .T. ) ;
#17512=ADVANCED_FACE ( 'NONE', ( #11293 ), #37469, .F. ) ;
#17561=CARTESIAN_POINT ( 'NONE',  ( 12.49999999999999822, -120.0000000000000000, -125.0000000000000000 ) ) ;
#17845=VERTEX_POINT ( 'NONE', #45241 ) ;
#17872=STYLED_ITEM ( 'NONE', ( #29609 ), #38066 ) ;
#17922=CARTESIAN_POINT ( 'NONE',  ( -12.50000000000000000, -107.5000000000000000, 40.00000000000000000 ) ) ;
#17943=CARTESIAN_POINT ( 'NONE',  ( 0.000000000000000000, -120.0000000000000000, 125.0000000000000000 ) ) ;
#18016=PLANE ( 'NONE',  #34243 ) ;
#18217=EDGE_CURVE ( 'NONE', #37702, #17845, #30467, .T. ) ;
#18240=EDGE_CURVE ( 'NONE', #39340, #35947, #27015, .T. ) ;
#18693=FACE_OUTER_BOUND ( 'NONE', #13622, .T. ) ;
#18749=DIRECTION ( 'NONE',  ( -0.000000000000000000, -0.000000000000000000, -1.000000000000000000 ) ) ;
#18826=PRODUCT_DEFINITION_CONTEXT ( 'detailed design', #30723, 'design' ) ;
#18860=ORIENTED_EDGE ( 'NONE', *, *, #18217, .F. ) ;
#19008=VECTOR ( 'NONE', #25612, 1000.000000000000000 ) ;
#19133=DIRECTION ( 'NONE',  ( -0.000000000000000000, -1.000000000000000000, -0.000000000000000000 ) ) ;
#19158=DIRECTION ( 'NONE',  ( -0.000000000000000000, -0.000000000000000000, -1.000000000000000000 ) ) ;
#19160=ORIENTED_EDGE ( 'NONE', *, *, #45366, .T. ) ;
#19360=DIRECTION ( 'NONE',  ( -0.000000000000000000, -0.000000000000000000, -1.000000000000000000 ) ) ;
#19483=DIRECTION ( 'NONE',  ( -1.000000000000000000, 0.000000000000000000, 0.000000000000000000 ) ) ;
#19487=AXIS2_PLACEMENT_3D ( 'NONE', #11557, #46051, #30162 ) ;
#19498=ORIENTED_EDGE ( 'NONE', *, *, #11274, .T. ) ;
#19554=EDGE_CURVE ( 'NONE', #25578, #5318, #34895, .T. ) ;
#19620=AXIS2_PLACEMENT_3D ( 'NONE', #6910, #7865, #48018 ) ;
#19727=EDGE_CURVE ( 'NONE', #17845, #9989, #43791, .T. ) ;
#19909=EDGE_CURVE ( 'NONE', #13681, #16544, #25471, .T. ) ;
#19912=MANIFOLD_SOLID_BREP ( 'Boss-Extrude2', #40364 ) ;
#19915=AXIS2_PLACEMENT_3D ( 'NONE', #35693, #20269, #46226 ) ;
#20187=DIRECTION ( 'NONE',  ( 0.000000000000000000, 0.000000000000000000, 1.000000000000000000 ) ) ;
#20269=DIRECTION ( 'NONE',  ( 0.000000000000000000, 0.000000000000000000, -1.000000000000000000 ) ) ;
#20287=LINE ( 'NONE', #28361, #46475 ) ;
#20563=CARTESIAN_POINT ( 'NONE',  ( 12.50000000000000000, -132.5000000000000000, -40.00000000000000000 ) ) ;
#20622=AXIS2_PLACEMENT_3D ( 'NONE', #31733, #27319, #24124 ) ;
#20665=EDGE_CURVE ( 'NONE', #7974, #42505, #2608, .T. ) ;
#20749=DIRECTION ( 'NONE',  ( 0.000000000000000000, 0.000000000000000000, -1.000000000000000000 ) ) ;
#20762=PLANE ( 'NONE',  #19915 ) ;
#20789=EDGE_CURVE ( 'NONE', #16544, #4123, #30028, .T. ) ;
#20851=PLANE ( 'NONE',  #6556 ) ;
#21112=EDGE_LOOP ( 'NONE', ( #3929, #39093, #39602, #12399, #15835, #10432 ) ) ;
#21354=CARTESIAN_POINT ( 'NONE',  ( 12.49999999999999822, -120.0000000000000000, 125.0000000000000000 ) ) ;
#21416=DIRECTION ( 'NONE',  ( 0.000000000000000000, 0.000000000000000000, -1.000000000000000000 ) ) ;
#21536=ORIENTED_EDGE ( 'NONE', *, *, #41321, .F. ) ;
#21575=EDGE_LOOP ( 'NONE', ( #28498, #2796, #12473, #17207, #42594 ) ) ;
#21636=CYLINDRICAL_SURFACE ( 'NONE', #15263, 12.49999999999999822 ) ;
#21683=EDGE_CURVE ( 'NONE', #6694, #17845, #37431, .T. ) ;
#21704=ADVANCED_FACE ( 'NONE', ( #44770 ), #3899, .T. ) ;
#21796=( LENGTH_UNIT ( ) NAMED_UNIT ( * ) SI_UNIT ( .MILLI., .METRE. ) );
#21816=DIRECTION ( 'NONE',  ( 0.000000000000000000, 0.000000000000000000, -1.000000000000000000 ) ) ;
#21927=DIRECTION ( 'NONE',  ( 0.000000000000000000, 1.000000000000000000, 0.000000000000000000 ) ) ;
#22016=SURFACE_SIDE_STYLE ('',( #7090 ) ) ;
#22045=LINE ( 'NONE', #2727, #5613 ) ;
#22060=AXIS2_PLACEMENT_3D ( 'NONE', #22935, #38117, #19483 ) ;
#22077=DIRECTION ( 'NONE',  ( -1.000000000000000000, 0.000000000000000000, 0.000000000000000000 ) ) ;
#22105=CARTESIAN_POINT ( 'NONE',  ( 12.50000000000000000, -132.5000000000000000, 40.00000000000000000 ) ) ;
#22126=DIRECTION ( 'NONE',  ( -0.000000000000000000, -0.000000000000000000, -1.000000000000000000 ) ) ;
#22181=ORIENTED_EDGE ( 'NONE', *, *, #41842, .T. ) ;
#22265=CARTESIAN_POINT ( 'NONE',  ( 0.000000000000000000, 0.000000000000000000, -40.00000000000000000 ) ) ;
#22386=DIRECTION ( 'NONE',  ( 0.000000000000000000, -0.000000000000000000, -1.000000000000000000 ) ) ;
#22428=CARTESIAN_POINT ( 'NONE',  ( 12.50000000000000000, -132.5000000000000000, 40.00000000000000000 ) ) ;
#22566=CARTESIAN_POINT ( 'NONE',  ( 0.000000000000000000, -120.0000000000000000, 40.00000000000000711 ) ) ;
#22579=APPLICATION_CONTEXT ( 'automotive_design' ) ;
#22709=LINE ( 'NONE', #33964, #31376 ) ;
#22810=AXIS2_PLACEMENT_3D ( 'NONE', #26949, #26457, #26698 ) ;
#22935=CARTESIAN_POINT ( 'NONE',  ( 0.000000000000000000, -120.0000000000000000, 125.0000000000000000 ) ) ;
#22976=ORIENTED_EDGE ( 'NONE', *, *, #14915, .T. ) ;
#22990=ORIENTED_EDGE ( 'NONE', *, *, #27129, .T. ) ;
#23039=LINE ( 'NONE', #996, #40962 ) ;
#23069=AXIS2_PLACEMENT_3D ( 'NONE', #32031, #29965, #24675 ) ;
#23181=FACE_OUTER_BOUND ( 'NONE', #21575, .T. ) ;
#23246=EDGE_LOOP ( 'NONE', ( #37161, #38295, #43067 ) ) ;
#23326=DIRECTION ( 'NONE',  ( 0.000000000000000000, 1.000000000000000000, 0.000000000000000000 ) ) ;
#23366=( GEOMETRIC_REPRESENTATION_CONTEXT ( 3 ) GLOBAL_UNCERTAINTY_ASSIGNED_CONTEXT ( ( #718 ) ) GLOBAL_UNIT_ASSIGNED_CONTEXT ( ( #46005, #1208, #8056 ) ) REPRESENTATION_CONTEXT ( 'NONE', 'WORKASPACE' ) );
#23490=COLOUR_RGB ( '', 0.31764706, 0.68627451, 0.89019608) ;
#23496=VERTEX_POINT ( 'NONE', #41599 ) ;
#23547=CIRCLE ( 'NONE', #19620, 12.49999999999999822 ) ;
#23670=VECTOR ( 'NONE', #33623, 1000.000000000000000 ) ;
#24124=DIRECTION ( 'NONE',  ( -1.000000000000000000, 0.000000000000000000, -0.000000000000000000 ) ) ;
#24301=CARTESIAN_POINT ( 'NONE',  ( 0.000000000000000000, -132.5000000000000000, 40.00000000000000711 ) ) ;
#24338=ORIENTED_EDGE ( 'NONE', *, *, #28584, .T. ) ;
#24351=CARTESIAN_POINT ( 'NONE',  ( 12.50000000000000000, -120.0000000000000000, -40.00000000000000711 ) ) ;
#24422=FACE_OUTER_BOUND ( 'NONE', #30743, .T. ) ;
#24524=VERTEX_POINT ( 'NONE', #25897 ) ;
#24675=DIRECTION ( 'NONE',  ( -1.000000000000000000, 0.000000000000000000, 0.000000000000000000 ) ) ;
#24763=CARTESIAN_POINT ( 'NONE',  ( -12.50000000000000000, -132.5000000000000000, 40.00000000000000000 ) ) ;
#25021=DIRECTION ( 'NONE',  ( 1.000000000000000000, 0.000000000000000000, -0.000000000000000000 ) ) ;
#25027=LINE ( 'NONE', #21354, #36437 ) ;
#25073=DIRECTION ( 'NONE',  ( -1.000000000000000000, 0.000000000000000000, 0.000000000000000000 ) ) ;
#25214=SURFACE_STYLE_FILL_AREA ( #6165 ) ;
#25243=EDGE_CURVE ( 'NONE', #9989, #28782, #36332, .T. ) ;
#25251=CARTESIAN_POINT ( 'NONE',  ( 0.000000000000000000, -120.0000000000000000, 125.0000000000000000 ) ) ;
#25471=LINE ( 'NONE', #36251, #9447 ) ;
#25578=VERTEX_POINT ( 'NONE', #31421 ) ;
#25600=PLANE ( 'NONE',  #64 ) ;
#25612=DIRECTION ( 'NONE',  ( 1.000000000000000000, 0.000000000000000000, 0.000000000000000000 ) ) ;
#25686=ADVANCED_FACE ( 'NONE', ( #28918 ), #36985, .F. ) ;
#25894=VECTOR ( 'NONE', #28815, 1000.000000000000000 ) ;
#25897=CARTESIAN_POINT ( 'NONE',  ( -12.50000000000000000, -120.0000000000000000, 40.00000000000000711 ) ) ;
#26045=PLANE ( 'NONE',  #13506 ) ;
#26155=ORIENTED_EDGE ( 'NONE', *, *, #21683, .T. ) ;
#26245=CARTESIAN_POINT ( 'NONE',  ( 12.49999999999999822, -120.0000000000000000, 125.0000000000000000 ) ) ;
#26292=FACE_OUTER_BOUND ( 'NONE', #30998, .T. ) ;
#26297=CARTESIAN_POINT ( 'NONE',  ( 12.50000000000000000, -132.5000000000000000, 40.00000000000000000 ) ) ;
#26407=VECTOR ( 'NONE', #6688, 1000.000000000000000 ) ;
#26457=DIRECTION ( 'NONE',  ( 0.000000000000000000, 0.000000000000000000, 1.000000000000000000 ) ) ;
#26534=ADVANCED_FACE ( 'NONE', ( #18693 ), #26045, .F. ) ;
#26536=EDGE_CURVE ( 'NONE', #39340, #42505, #29959, .T. ) ;
#26608=AXIS2_PLACEMENT_3D ( 'NONE', #12145, #8675, #41749 ) ;
#26646=( GEOMETRIC_REPRESENTATION_CONTEXT ( 3 ) GLOBAL_UNCERTAINTY_ASSIGNED_CONTEXT ( ( #34007 ) ) GLOBAL_UNIT_ASSIGNED_CONTEXT ( ( #21796, #13975, #47733 ) ) REPRESENTATION_CONTEXT ( 'NONE', 'WORKASPACE' ) );
#26698=DIRECTION ( 'NONE',  ( 1.000000000000000000, 0.000000000000000000, -0.000000000000000000 ) ) ;
#26731=CYLINDRICAL_SURFACE ( 'NONE', #1427, 12.49999999999999822 ) ;
#26938=ORIENTED_EDGE ( 'NONE', *, *, #19909, .F. ) ;
#26949=CARTESIAN_POINT ( 'NONE',  ( 0.000000000000000000, -120.0000000000000000, -125.0000000000000000 ) ) ;
#27015=LINE ( 'NONE', #16241, #29650 ) ;
#27019=ORIENTED_EDGE ( 'NONE', *, *, #35214, .F. ) ;
#27129=EDGE_CURVE ( 'NONE', #13681, #35947, #13259, .T. ) ;
#27295=MECHANICAL_DESIGN_GEOMETRIC_PRESENTATION_REPRESENTATION('',(#17872),#23366);
#27319=DIRECTION ( 'NONE',  ( 0.000000000000000000, 0.000000000000000000, -1.000000000000000000 ) ) ;
#27807=EDGE_CURVE ( 'NONE', #7974, #37702, #10173, .T. ) ;
#27884=CARTESIAN_POINT ( 'NONE',  ( -12.50000000000000000, -132.5000000000000000, -40.00000000000000000 ) ) ;
#27976=EDGE_CURVE ( 'NONE', #39765, #34109, #30539, .T. ) ;
#28137=ORIENTED_EDGE ( 'NONE', *, *, #28584, .F. ) ;
#28204=ORIENTED_EDGE ( 'NONE', *, *, #44715, .T. ) ;
#28207=ORIENTED_EDGE ( 'NONE', *, *, #27976, .F. ) ;
#28222=PLANE ( 'NONE',  #4409 ) ;
#28286=ORIENTED_EDGE ( 'NONE', *, *, #46710, .F. ) ;
#28304=PRODUCT_DEFINITION ( 'UNKNOWN', '', #45220, #18826 ) ;
#28322=DIRECTION ( 'NONE',  ( -1.000000000000000000, 0.000000000000000000, -0.000000000000000000 ) ) ;
#28361=CARTESIAN_POINT ( 'NONE',  ( -12.50000000000000000, -107.5000000000000000, -40.00000000000000000 ) ) ;
#28466=EDGE_CURVE ( 'NONE', #37765, #28782, #23547, .T. ) ;
#28468=ORIENTED_EDGE ( 'NONE', *, *, #21683, .F. ) ;
#28498=ORIENTED_EDGE ( 'NONE', *, *, #19727, .T. ) ;
#28535=AXIS2_PLACEMENT_3D ( 'NONE', #4270, #41956, #38510 ) ;
#28584=EDGE_CURVE ( 'NONE', #35947, #5318, #15727, .T. ) ;
#28782=VERTEX_POINT ( 'NONE', #17561 ) ;
#28815=DIRECTION ( 'NONE',  ( 1.000000000000000000, 0.000000000000000000, 0.000000000000000000 ) ) ;
#28870=DIRECTION ( 'NONE',  ( -0.000000000000000000, -1.000000000000000000, -0.000000000000000000 ) ) ;
#28918=FACE_OUTER_BOUND ( 'NONE', #15269, .T. ) ;
#29052=DIRECTION ( 'NONE',  ( -0.000000000000000000, -0.000000000000000000, -1.000000000000000000 ) ) ;
#29173=DIRECTION ( 'NONE',  ( 0.000000000000000000, 0.000000000000000000, -1.000000000000000000 ) ) ;
#29205=DIRECTION ( 'NONE',  ( -1.000000000000000000, 0.000000000000000000, -0.000000000000000000 ) ) ;
#29540=CARTESIAN_POINT ( 'NONE',  ( 12.50000000000000000, -107.5000000000000000, 40.00000000000000000 ) ) ;
#29609=PRESENTATION_STYLE_ASSIGNMENT (( #48215 ) ) ;
#29650=VECTOR ( 'NONE', #23326, 1000.000000000000000 ) ;
#29959=LINE ( 'NONE', #26297, #23670 ) ;
#29965=DIRECTION ( 'NONE',  ( 0.000000000000000000, 0.000000000000000000, -1.000000000000000000 ) ) ;
#30028=LINE ( 'NONE', #3839, #3251 ) ;
#30162=DIRECTION ( 'NONE',  ( -1.000000000000000000, 0.000000000000000000, 0.000000000000000000 ) ) ;
#30165=DIRECTION ( 'NONE',  ( -0.000000000000000000, -1.000000000000000000, -0.000000000000000000 ) ) ;
#30426=LINE ( 'NONE', #22105, #39921 ) ;
#30467=CIRCLE ( 'NONE', #42980, 12.49999999999999822 ) ;
#30539=CIRCLE ( 'NONE', #14129, 12.49999999999999822 ) ;
#30650=PRODUCT_CONTEXT ( 'NONE', #22579, 'mechanical' ) ;
#30723=APPLICATION_CONTEXT ( 'automotive_design' ) ;
#30743=EDGE_LOOP ( 'NONE', ( #39896, #19498, #34940 ) ) ;
#30874=CIRCLE ( 'NONE', #23069, 12.49999999999999822 ) ;
#30998=EDGE_LOOP ( 'NONE', ( #4834, #28468, #832 ) ) ;
#31156=CARTESIAN_POINT ( 'NONE',  ( 0.000000000000000000, -120.0000000000000000, -40.00000000000000711 ) ) ;
#31349=ORIENTED_EDGE ( 'NONE', *, *, #41321, .T. ) ;
#31376=VECTOR ( 'NONE', #34682, 1000.000000000000000 ) ;
#31421=CARTESIAN_POINT ( 'NONE',  ( -12.50000000000000000, -132.5000000000000000, 40.00000000000000000 ) ) ;
#31564=VECTOR ( 'NONE', #19360, 1000.000000000000000 ) ;
#31700=EDGE_CURVE ( 'NONE', #6714, #6694, #11667, .T. ) ;
#31733=CARTESIAN_POINT ( 'NONE',  ( 0.000000000000000000, 0.000000000000000000, 40.00000000000000000 ) ) ;
#32031=CARTESIAN_POINT ( 'NONE',  ( 0.000000000000000000, -120.0000000000000000, -40.00000000000000711 ) ) ;
#32384=PRODUCT_DEFINITION_SHAPE ( 'NONE', 'NONE',  #28304 ) ;
#32615=FACE_OUTER_BOUND ( 'NONE', #40383, .T. ) ;
#32674=FACE_OUTER_BOUND ( 'NONE', #37174, .T. ) ;
#32814=DIRECTION ( 'NONE',  ( 1.000000000000000000, 0.000000000000000000, 0.000000000000000000 ) ) ;
#33228=LINE ( 'NONE', #14639, #12250 ) ;
#33276=CARTESIAN_POINT ( 'NONE',  ( -12.50000000000000000, -107.5000000000000000, -40.00000000000000000 ) ) ;
#33342=CARTESIAN_POINT ( 'NONE',  ( -12.50000000000000000, -132.5000000000000000, -40.00000000000000000 ) ) ;
#33537=ORIENTED_EDGE ( 'NONE', *, *, #27129, .F. ) ;
#33623=DIRECTION ( 'NONE',  ( -0.000000000000000000, -0.000000000000000000, -1.000000000000000000 ) ) ;
#33832=ORIENTED_EDGE ( 'NONE', *, *, #34174, .T. ) ;
#33885=ORIENTED_EDGE ( 'NONE', *, *, #26536, .F. ) ;
#33964=CARTESIAN_POINT ( 'NONE',  ( 12.50000000000000000, -132.5000000000000000, -40.00000000000000000 ) ) ;
#34007=UNCERTAINTY_MEASURE_WITH_UNIT (LENGTH_MEASURE( 1.000000000000000082E-05 ), #21796, 'distance_accuracy_value', 'NONE');
#34016=ADVANCED_FACE ( 'NONE', ( #32615 ), #28222, .T. ) ;
#34109=VERTEX_POINT ( 'NONE', #26245 ) ;
#34174=EDGE_CURVE ( 'NONE', #37702, #23496, #44356, .T. ) ;
#34228=DIRECTION ( 'NONE',  ( 0.000000000000000000, 0.000000000000000000, -1.000000000000000000 ) ) ;
#34243=AXIS2_PLACEMENT_3D ( 'NONE', #6782, #20749, #28322 ) ;
#34417=MECHANICAL_DESIGN_GEOMETRIC_PRESENTATION_REPRESENTATION('',(#7879),#26646);
#34620=VECTOR ( 'NONE', #14684, 1000.000000000000000 ) ;
#34682=DIRECTION ( 'NONE',  ( 0.000000000000000000, 1.000000000000000000, 0.000000000000000000 ) ) ;
#34895=LINE ( 'NONE', #39057, #10152 ) ;
#34940=ORIENTED_EDGE ( 'NONE', *, *, #19909, .T. ) ;
#35108=DIRECTION ( 'NONE',  ( 1.000000000000000000, 0.000000000000000000, 0.000000000000000000 ) ) ;
#35181=ORIENTED_EDGE ( 'NONE', *, *, #31700, .T. ) ;
#35194=ORIENTED_EDGE ( 'NONE', *, *, #41246, .F. ) ;
#35214=EDGE_CURVE ( 'NONE', #6714, #13681, #39070, .T. ) ;
#35283=DIRECTION ( 'NONE',  ( 0.000000000000000000, 0.000000000000000000, -1.000000000000000000 ) ) ;
#35364=ADVANCED_FACE ( 'NONE', ( #3977 ), #26731, .T. ) ;
#35622=FACE_OUTER_BOUND ( 'NONE', #44676, .T. ) ;
#35693=CARTESIAN_POINT ( 'NONE',  ( 0.000000000000000000, 0.000000000000000000, 40.00000000000000000 ) ) ;
#35850=ADVANCED_FACE ( 'NONE', ( #13887 ), #18016, .T. ) ;
#35947=VERTEX_POINT ( 'NONE', #17062 ) ;
#36032=AXIS2_PLACEMENT_3D ( 'NONE', #40836, #44742, #4121 ) ;
#36095=CARTESIAN_POINT ( 'NONE',  ( 0.000000000000000000, -120.0000000000000000, 125.0000000000000000 ) ) ;
#36210=AXIS2_PLACEMENT_3D ( 'NONE', #11349, #40957, #29205 ) ;
#36251=CARTESIAN_POINT ( 'NONE',  ( -12.50000000000000000, -107.5000000000000000, 40.00000000000000000 ) ) ;
#36332=LINE ( 'NONE', #11112, #45126 ) ;
#36437=VECTOR ( 'NONE', #43877, 1000.000000000000000 ) ;
#36704=( NAMED_UNIT ( * ) SI_UNIT ( $, .STERADIAN. ) SOLID_ANGLE_UNIT ( ) );
#36762=AXIS2_PLACEMENT_3D ( 'NONE', #36095, #22126, #25073 ) ;
#36813=CARTESIAN_POINT ( 'NONE',  ( -12.50000000000000000, -107.5000000000000000, 40.00000000000000000 ) ) ;
#36985=PLANE ( 'NONE',  #14659 ) ;
#37029=FACE_OUTER_BOUND ( 'NONE', #23246, .T. ) ;
#37161=ORIENTED_EDGE ( 'NONE', *, *, #45366, .F. ) ;
#37174=EDGE_LOOP ( 'NONE', ( #14329, #24338, #6942 ) ) ;
#37190=DIRECTION ( 'NONE',  ( 0.000000000000000000, 0.000000000000000000, -1.000000000000000000 ) ) ;
#37258=FACE_OUTER_BOUND ( 'NONE', #21112, .T. ) ;
#37431=LINE ( 'NONE', #33276, #34620 ) ;
#37469=PLANE ( 'NONE',  #22810 ) ;
#37702=VERTEX_POINT ( 'NONE', #39090 ) ;
#37765=VERTEX_POINT ( 'NONE', #42277 ) ;
#38066=ADVANCED_BREP_SHAPE_REPRESENTATION ( '', ( #19912, #11636 ), #38234 ) ;
#38117=DIRECTION ( 'NONE',  ( -0.000000000000000000, -0.000000000000000000, -1.000000000000000000 ) ) ;
#38234=( GEOMETRIC_REPRESENTATION_CONTEXT ( 3 ) GLOBAL_UNCERTAINTY_ASSIGNED_CONTEXT ( ( #4637 ) ) GLOBAL_UNIT_ASSIGNED_CONTEXT ( ( #47711, #40402, #36704 ) ) REPRESENTATION_CONTEXT ( 'NONE', 'WORKASPACE' ) );
#38295=ORIENTED_EDGE ( 'NONE', *, *, #38888, .F. ) ;
#38318=ORIENTED_EDGE ( 'NONE', *, *, #25243, .F. ) ;
#38470=EDGE_CURVE ( 'NONE', #35947, #6714, #30426, .T. ) ;
#38510=DIRECTION ( 'NONE',  ( -1.000000000000000000, 0.000000000000000000, -0.000000000000000000 ) ) ;
#38554=CARTESIAN_POINT ( 'NONE',  ( -12.50000000000000000, -107.5000000000000000, 40.00000000000000000 ) ) ;
#38627=DIRECTION ( 'NONE',  ( 1.000000000000000000, 0.000000000000000000, 0.000000000000000000 ) ) ;
#38718=DIRECTION ( 'NONE',  ( -1.000000000000000000, 0.000000000000000000, 0.000000000000000000 ) ) ;
#38888=EDGE_CURVE ( 'NONE', #42505, #9989, #22709, .T. ) ;
#39057=CARTESIAN_POINT ( 'NONE',  ( -12.50000000000000000, -132.5000000000000000, 40.00000000000000000 ) ) ;
#39070=LINE ( 'NONE', #17922, #26407 ) ;
#39090=CARTESIAN_POINT ( 'NONE',  ( -12.50000000000000000, -120.0000000000000000, -40.00000000000000711 ) ) ;
#39093=ORIENTED_EDGE ( 'NONE', *, *, #18240, .F. ) ;
#39137=ADVANCED_FACE ( 'NONE', ( #10694 ), #25600, .F. ) ;
#39340=VERTEX_POINT ( 'NONE', #22428 ) ;
#39602=ORIENTED_EDGE ( 'NONE', *, *, #26536, .T. ) ;
#39636=ORIENTED_EDGE ( 'NONE', *, *, #20789, .T. ) ;
#39709=DIRECTION ( 'NONE',  ( -1.000000000000000000, -0.000000000000000000, -0.000000000000000000 ) ) ;
#39765=VERTEX_POINT ( 'NONE', #48305 ) ;
#39896=ORIENTED_EDGE ( 'NONE', *, *, #46710, .T. ) ;
#39921=VECTOR ( 'NONE', #11820, 1000.000000000000000 ) ;
#39934=DIRECTION ( 'NONE',  ( 1.000000000000000000, 0.000000000000000000, 0.000000000000000000 ) ) ;
#39981=CARTESIAN_POINT ( 'NONE',  ( 12.50000000000000000, -107.5000000000000000, -40.00000000000000000 ) ) ;
#40252=FACE_OUTER_BOUND ( 'NONE', #1848, .T. ) ;
#40364=CLOSED_SHELL ( 'NONE', ( #13492, #16975, #35364, #34016, #6907, #26534, #15704, #39137, #45267, #25686, #3816, #21704, #44257, #15386, #9949, #35850, #17512, #5114 ) ) ;
#40383=EDGE_LOOP ( 'NONE', ( #4760, #31349 ) ) ;
#40402=( NAMED_UNIT ( * ) PLANE_ANGLE_UNIT ( ) SI_UNIT ( $, .RADIAN. ) );
#40626=FILL_AREA_STYLE ('',( #10777 ) ) ;
#40644=SURFACE_STYLE_USAGE ( .BOTH. , #2471 ) ;
#40702=PLANE ( 'NONE',  #36210 ) ;
#40745=CARTESIAN_POINT ( 'NONE',  ( 0.000000000000000000, 0.000000000000000000, 40.00000000000000000 ) ) ;
#40836=CARTESIAN_POINT ( 'NONE',  ( 0.000000000000000000, -120.0000000000000000, 40.00000000000000711 ) ) ;
#40918=CARTESIAN_POINT ( 'NONE',  ( 0.000000000000000000, 0.000000000000000000, 40.00000000000000000 ) ) ;
#40919=ORIENTED_EDGE ( 'NONE', *, *, #10924, .F. ) ;
#40957=DIRECTION ( 'NONE',  ( 0.000000000000000000, 0.000000000000000000, -1.000000000000000000 ) ) ;
#40962=VECTOR ( 'NONE', #8579, 1000.000000000000000 ) ;
#41190=PLANE ( 'NONE',  #5186 ) ;
#41246=EDGE_CURVE ( 'NONE', #5318, #24524, #9443, .T. ) ;
#41321=EDGE_CURVE ( 'NONE', #34109, #39765, #43897, .T. ) ;
#41349=ORIENTED_EDGE ( 'NONE', *, *, #20665, .T. ) ;
#41368=EDGE_LOOP ( 'NONE', ( #44576, #28207, #43948, #35194, #28137 ) ) ;
#41467=AXIS2_PLACEMENT_3D ( 'NONE', #31156, #5679, #5935 ) ;
#41599=CARTESIAN_POINT ( 'NONE',  ( -12.50000000000000000, -132.5000000000000000, -40.00000000000000000 ) ) ;
#41749=DIRECTION ( 'NONE',  ( -1.000000000000000000, 0.000000000000000000, 0.000000000000000000 ) ) ;
#41814=CARTESIAN_POINT ( 'NONE',  ( 0.000000000000000000, -120.0000000000000000, 125.0000000000000000 ) ) ;
#41842=EDGE_CURVE ( 'NONE', #37702, #37765, #22045, .T. ) ;
#41956=DIRECTION ( 'NONE',  ( 0.000000000000000000, 0.000000000000000000, -1.000000000000000000 ) ) ;
#42075=DIRECTION ( 'NONE',  ( -1.000000000000000000, 0.000000000000000000, 0.000000000000000000 ) ) ;
#42277=CARTESIAN_POINT ( 'NONE',  ( -12.49999999999999822, -120.0000000000000000, -125.0000000000000000 ) ) ;
#42415=DIRECTION ( 'NONE',  ( -1.000000000000000000, 0.000000000000000000, 0.000000000000000000 ) ) ;
#42505=VERTEX_POINT ( 'NONE', #5581 ) ;
#42594=ORIENTED_EDGE ( 'NONE', *, *, #18217, .T. ) ;
#42621=DIRECTION ( 'NONE',  ( 0.000000000000000000, 1.000000000000000000, 0.000000000000000000 ) ) ;
#42699=VECTOR ( 'NONE', #30165, 1000.000000000000000 ) ;
#42710=EDGE_CURVE ( 'NONE', #5318, #39340, #44231, .T. ) ;
#42714=EDGE_LOOP ( 'NONE', ( #2651, #28286, #39636, #7546, #33832, #9093 ) ) ;
#42746=CIRCLE ( 'NONE', #10697, 12.49999999999999822 ) ;
#42971=PLANE ( 'NONE',  #20622 ) ;
#42980=AXIS2_PLACEMENT_3D ( 'NONE', #12326, #8624, #42415 ) ;
#43067=ORIENTED_EDGE ( 'NONE', *, *, #20665, .F. ) ;
#43124=FACE_OUTER_BOUND ( 'NONE', #42714, .T. ) ;
#43160=DIRECTION ( 'NONE',  ( 0.000000000000000000, 0.000000000000000000, 1.000000000000000000 ) ) ;
#43614=DIRECTION ( 'NONE',  ( -0.000000000000000000, -0.000000000000000000, -1.000000000000000000 ) ) ;
#43791=CIRCLE ( 'NONE', #41467, 12.49999999999999822 ) ;
#43877=DIRECTION ( 'NONE',  ( -0.000000000000000000, -0.000000000000000000, -1.000000000000000000 ) ) ;
#43897=CIRCLE ( 'NONE', #6382, 12.49999999999999822 ) ;
#43944=CARTESIAN_POINT ( 'NONE',  ( 0.000000000000000000, -107.5000000000000000, 40.00000000000000711 ) ) ;
#43948=ORIENTED_EDGE ( 'NONE', *, *, #17092, .T. ) ;
#44129=VECTOR ( 'NONE', #18749, 1000.000000000000000 ) ;
#44150=DIRECTION ( 'NONE',  ( -1.000000000000000000, 0.000000000000000000, 0.000000000000000000 ) ) ;
#44231=LINE ( 'NONE', #10706, #19008 ) ;
#44257=ADVANCED_FACE ( 'NONE', ( #26292 ), #45135, .T. ) ;
#44326=FILL_AREA_STYLE_COLOUR ( '', #23490 ) ;
#44356=LINE ( 'NONE', #33342, #42699 ) ;
#44359=ORIENTED_EDGE ( 'NONE', *, *, #5652, .T. ) ;
#44402=DIRECTION ( 'NONE',  ( -0.000000000000000000, -0.000000000000000000, -1.000000000000000000 ) ) ;
#44482=ORIENTED_EDGE ( 'NONE', *, *, #19554, .T. ) ;
#44576=ORIENTED_EDGE ( 'NONE', *, *, #6697, .F. ) ;
#44676=EDGE_LOOP ( 'NONE', ( #44482, #5695, #15859 ) ) ;
#44715=EDGE_CURVE ( 'NONE', #23496, #7974, #23039, .T. ) ;
#44742=DIRECTION ( 'NONE',  ( 0.000000000000000000, 0.000000000000000000, -1.000000000000000000 ) ) ;
#44770=FACE_OUTER_BOUND ( 'NONE', #498, .T. ) ;
#45126=VECTOR ( 'NONE', #44402, 1000.000000000000000 ) ;
#45135=PLANE ( 'NONE',  #28535 ) ;
#45220=PRODUCT_DEFINITION_FORMATION_WITH_SPECIFIED_SOURCE ( 'ANY', '', #47219, .NOT_KNOWN. ) ;
#45241=CARTESIAN_POINT ( 'NONE',  ( 0.000000000000000000, -107.5000000000000000, -40.00000000000000711 ) ) ;
#45267=ADVANCED_FACE ( 'NONE', ( #24422 ), #20762, .F. ) ;
#45317=CARTESIAN_POINT ( 'NONE',  ( 12.50000000000000000, -132.5000000000000000, 40.00000000000000000 ) ) ;
#45366=EDGE_CURVE ( 'NONE', #9989, #7974, #30874, .T. ) ;
#45552=DIRECTION ( 'NONE',  ( -1.000000000000000000, 0.000000000000000000, 0.000000000000000000 ) ) ;
#46005=( LENGTH_UNIT ( ) NAMED_UNIT ( * ) SI_UNIT ( .MILLI., .METRE. ) );
#46051=DIRECTION ( 'NONE',  ( 0.000000000000000000, 0.000000000000000000, -1.000000000000000000 ) ) ;
#46199=DIRECTION ( 'NONE',  ( 0.000000000000000000, 0.000000000000000000, 1.000000000000000000 ) ) ;
#46226=DIRECTION ( 'NONE',  ( -1.000000000000000000, 0.000000000000000000, -0.000000000000000000 ) ) ;
#46475=VECTOR ( 'NONE', #13437, 1000.000000000000000 ) ;
#46710=EDGE_CURVE ( 'NONE', #16544, #24524, #33228, .T. ) ;
#46864=CARTESIAN_POINT ( 'NONE',  ( 0.000000000000000000, -120.0000000000000000, 125.0000000000000000 ) ) ;
#47219=PRODUCT ( 'output shaft', 'output shaft', '', ( #30650 ) ) ;
#47543=CARTESIAN_POINT ( 'NONE',  ( 12.50000000000000000, -107.5000000000000000, 40.00000000000000000 ) ) ;
#47600=DIRECTION ( 'NONE',  ( -1.000000000000000000, 0.000000000000000000, -0.000000000000000000 ) ) ;
#47701=CARTESIAN_POINT ( 'NONE',  ( -12.50000000000000000, -132.5000000000000000, -40.00000000000000000 ) ) ;
#47711=( LENGTH_UNIT ( ) NAMED_UNIT ( * ) SI_UNIT ( .MILLI., .METRE. ) );
#47733=( NAMED_UNIT ( * ) SI_UNIT ( $, .STERADIAN. ) SOLID_ANGLE_UNIT ( ) );
#47802=DIRECTION ( 'NONE',  ( -0.000000000000000000, -0.000000000000000000, -1.000000000000000000 ) ) ;
#47988=ORIENTED_EDGE ( 'NONE', *, *, #17092, .F. ) ;
#48018=DIRECTION ( 'NONE',  ( 1.000000000000000000, 0.000000000000000000, 0.000000000000000000 ) ) ;
#48077=FACE_OUTER_BOUND ( 'NONE', #48278, .T. ) ;
#48109=EDGE_LOOP ( 'NONE', ( #6508, #16900, #10628 ) ) ;
#48124=DIRECTION ( 'NONE',  ( 0.000000000000000000, -0.000000000000000000, 1.000000000000000000 ) ) ;
#48215=SURFACE_STYLE_USAGE ( .BOTH. , #22016 ) ;
#48272=LINE ( 'NONE', #8114, #493 ) ;
#48278=EDGE_LOOP ( 'NONE', ( #38318, #19160, #3802, #22181, #12248 ) ) ;
#48305=CARTESIAN_POINT ( 'NONE',  ( -12.49999999999999822, -120.0000000000000000, 125.0000000000000000 ) ) ;
ENDSEC;
END-ISO-10303-21;
